ISO-10303-21;
HEADER;
/* Generated by software containing ST-Developer
 * from STEP Tools, Inc. (www.steptools.com) 
 */

FILE_DESCRIPTION(
/* description */ ('', 'CAx-IF Rec.Pracs.---Representation and Presentation of Product Manufa
cturing Information (PMI)---4.0---2014-10-13'),
/* implementation_level */ '2;1');

FILE_NAME(
/* name */ 'Chamber Hex Head Bolts.step',
/* time_stamp */ '2026-10-28T23:00:48+01:00',
/* author */ (''),
/* organization */ (''),
/* preprocessor_version */ 'ST-DEVELOPER v20.2',
/* originating_system */ 'Autodesk Translation Framework v15.17.0.0',
/* authorisation */ '');

FILE_SCHEMA (('AP242_MANAGED_MODEL_BASED_3D_ENGINEERING_MIM_LF { 1 0 10303 442 2 1 4 }'));
ENDSEC;

DATA;
#10=MECHANICAL_DESIGN_GEOMETRIC_PRESENTATION_REPRESENTATION('',(#966),#61811);
#497=(
BOUNDED_CURVE()
B_SPLINE_CURVE(2,(#51253,#51254,#51255),.UNSPECIFIED.,.F.,.F.)
B_SPLINE_CURVE_WITH_KNOTS((3,3),(0.46856777502019,0.937135550040381),
 .UNSPECIFIED.)
CURVE()
GEOMETRIC_REPRESENTATION_ITEM()
RATIONAL_B_SPLINE_CURVE((1.,1.03795484930203,1.))
REPRESENTATION_ITEM('')
);
#498=(
BOUNDED_CURVE()
B_SPLINE_CURVE(2,(#51258,#51259,#51260),.UNSPECIFIED.,.F.,.F.)
B_SPLINE_CURVE_WITH_KNOTS((3,3),(0.,0.468567775020191),.UNSPECIFIED.)
CURVE()
GEOMETRIC_REPRESENTATION_ITEM()
RATIONAL_B_SPLINE_CURVE((1.,1.03795484930204,1.))
REPRESENTATION_ITEM('')
);
#499=(
BOUNDED_CURVE()
B_SPLINE_CURVE(2,(#51264,#51265,#51266),.UNSPECIFIED.,.F.,.F.)
B_SPLINE_CURVE_WITH_KNOTS((3,3),(0.,0.468567775020191),.UNSPECIFIED.)
CURVE()
GEOMETRIC_REPRESENTATION_ITEM()
RATIONAL_B_SPLINE_CURVE((1.,1.03795484930204,1.))
REPRESENTATION_ITEM('')
);
#500=(
BOUNDED_CURVE()
B_SPLINE_CURVE(2,(#51267,#51268,#51269),.UNSPECIFIED.,.F.,.F.)
B_SPLINE_CURVE_WITH_KNOTS((3,3),(0.468567775020191,0.937135550040382),
 .UNSPECIFIED.)
CURVE()
GEOMETRIC_REPRESENTATION_ITEM()
RATIONAL_B_SPLINE_CURVE((1.,1.03795484930205,1.))
REPRESENTATION_ITEM('')
);
#501=(
BOUNDED_CURVE()
B_SPLINE_CURVE(2,(#51274,#51275,#51276),.UNSPECIFIED.,.F.,.F.)
B_SPLINE_CURVE_WITH_KNOTS((3,3),(0.468567775020191,0.937135550040382),
 .UNSPECIFIED.)
CURVE()
GEOMETRIC_REPRESENTATION_ITEM()
RATIONAL_B_SPLINE_CURVE((1.,1.03795484930204,1.))
REPRESENTATION_ITEM('')
);
#502=(
BOUNDED_CURVE()
B_SPLINE_CURVE(2,(#51278,#51279,#51280),.UNSPECIFIED.,.F.,.F.)
B_SPLINE_CURVE_WITH_KNOTS((3,3),(0.,0.46856777502019),.UNSPECIFIED.)
CURVE()
GEOMETRIC_REPRESENTATION_ITEM()
RATIONAL_B_SPLINE_CURVE((1.,1.03795484930204,1.))
REPRESENTATION_ITEM('')
);
#503=(
BOUNDED_CURVE()
B_SPLINE_CURVE(2,(#51284,#51285,#51286),.UNSPECIFIED.,.F.,.F.)
B_SPLINE_CURVE_WITH_KNOTS((3,3),(0.,0.468567775020191),.UNSPECIFIED.)
CURVE()
GEOMETRIC_REPRESENTATION_ITEM()
RATIONAL_B_SPLINE_CURVE((1.,1.03795484930203,1.))
REPRESENTATION_ITEM('')
);
#504=(
BOUNDED_CURVE()
B_SPLINE_CURVE(2,(#51287,#51288,#51289),.UNSPECIFIED.,.F.,.F.)
B_SPLINE_CURVE_WITH_KNOTS((3,3),(0.468567775020191,0.937135550040381),
 .UNSPECIFIED.)
CURVE()
GEOMETRIC_REPRESENTATION_ITEM()
RATIONAL_B_SPLINE_CURVE((1.,1.03795484930204,1.))
REPRESENTATION_ITEM('')
);
#505=(
BOUNDED_CURVE()
B_SPLINE_CURVE(2,(#51294,#51295,#51296),.UNSPECIFIED.,.F.,.F.)
B_SPLINE_CURVE_WITH_KNOTS((3,3),(0.468567775020191,0.937135550040381),
 .UNSPECIFIED.)
CURVE()
GEOMETRIC_REPRESENTATION_ITEM()
RATIONAL_B_SPLINE_CURVE((1.,1.03795484930203,1.))
REPRESENTATION_ITEM('')
);
#506=(
BOUNDED_CURVE()
B_SPLINE_CURVE(2,(#51298,#51299,#51300),.UNSPECIFIED.,.F.,.F.)
B_SPLINE_CURVE_WITH_KNOTS((3,3),(0.,0.468567775020191),.UNSPECIFIED.)
CURVE()
GEOMETRIC_REPRESENTATION_ITEM()
RATIONAL_B_SPLINE_CURVE((1.,1.03795484930204,1.))
REPRESENTATION_ITEM('')
);
#507=(
BOUNDED_CURVE()
B_SPLINE_CURVE(2,(#51303,#51304,#51305),.UNSPECIFIED.,.F.,.F.)
B_SPLINE_CURVE_WITH_KNOTS((3,3),(0.,0.468567775020191),.UNSPECIFIED.)
CURVE()
GEOMETRIC_REPRESENTATION_ITEM()
RATIONAL_B_SPLINE_CURVE((1.,1.03795484930203,1.))
REPRESENTATION_ITEM('')
);
#508=(
BOUNDED_CURVE()
B_SPLINE_CURVE(2,(#51306,#51307,#51308),.UNSPECIFIED.,.F.,.F.)
B_SPLINE_CURVE_WITH_KNOTS((3,3),(0.468567775020191,0.937135550040382),
 .UNSPECIFIED.)
CURVE()
GEOMETRIC_REPRESENTATION_ITEM()
RATIONAL_B_SPLINE_CURVE((1.,1.03795484930205,1.))
REPRESENTATION_ITEM('')
);
#571=CONICAL_SURFACE('',#34487,4.5399125,0.785343828859754);
#572=CONICAL_SURFACE('',#34490,8.618802153517,1.0471975511966);
#573=CONICAL_SURFACE('',#34492,8.618802153517,1.0471975511966);
#574=CONICAL_SURFACE('',#34494,8.618802153517,1.0471975511966);
#575=CONICAL_SURFACE('',#34496,8.618802153517,1.0471975511966);
#576=CONICAL_SURFACE('',#34498,8.618802153517,1.0471975511966);
#577=CONICAL_SURFACE('',#34500,8.618802153517,1.0471975511966);
#894=TOROIDAL_SURFACE('',#34477,5.4,0.4);
#916=SHAPE_REPRESENTATION_RELATIONSHIP('SRR','None',#61974,#941);
#941=ADVANCED_BREP_SHAPE_REPRESENTATION('',(#1005),#61787);
#966=STYLED_ITEM('',(#62163),#1005);
#1005=MANIFOLD_SOLID_BREP('Body1',#33796);
#1099=CYLINDRICAL_SURFACE('',#34482,5.);
#1100=CYLINDRICAL_SURFACE('',#34511,7.3);
#1903=FACE_BOUND('',#6323,.T.);
#1904=FACE_BOUND('',#6336,.T.);
#2421=CIRCLE('',#34478,5.);
#2422=CIRCLE('',#34479,5.);
#2423=CIRCLE('',#34480,0.4);
#2424=CIRCLE('',#34481,5.4);
#2425=CIRCLE('',#34483,5.);
#2426=CIRCLE('',#34484,5.);
#2427=CIRCLE('',#34486,7.3);
#2428=CIRCLE('',#34488,4.079825);
#2429=CIRCLE('',#34491,8.00000000000003);
#2430=CIRCLE('',#34493,8.00000000000003);
#2431=CIRCLE('',#34495,8.00000000000003);
#2432=CIRCLE('',#34497,8.00000000000003);
#2433=CIRCLE('',#34499,8.00000000000003);
#2434=CIRCLE('',#34501,8.00000000000003);
#2435=CIRCLE('',#34506,7.3);
#4417=FACE_OUTER_BOUND('',#6320,.T.);
#4418=FACE_OUTER_BOUND('',#6321,.T.);
#4419=FACE_OUTER_BOUND('',#6322,.T.);
#4420=FACE_OUTER_BOUND('',#6324,.T.);
#4421=FACE_OUTER_BOUND('',#6325,.T.);
#4422=FACE_OUTER_BOUND('',#6326,.T.);
#4423=FACE_OUTER_BOUND('',#6327,.T.);
#4424=FACE_OUTER_BOUND('',#6328,.T.);
#4425=FACE_OUTER_BOUND('',#6329,.T.);
#4426=FACE_OUTER_BOUND('',#6330,.T.);
#4427=FACE_OUTER_BOUND('',#6331,.T.);
#4428=FACE_OUTER_BOUND('',#6332,.T.);
#4429=FACE_OUTER_BOUND('',#6333,.T.);
#4430=FACE_OUTER_BOUND('',#6334,.T.);
#4431=FACE_OUTER_BOUND('',#6335,.T.);
#4432=FACE_OUTER_BOUND('',#6337,.T.);
#4433=FACE_OUTER_BOUND('',#6338,.T.);
#4434=FACE_OUTER_BOUND('',#6339,.T.);
#4435=FACE_OUTER_BOUND('',#6340,.T.);
#4436=FACE_OUTER_BOUND('',#6341,.T.);
#6320=EDGE_LOOP('',(#22298,#22299,#22300,#22301,#22302));
#6321=EDGE_LOOP('',(#22303,#22304,#22305,#22306,#22307,#22308));
#6322=EDGE_LOOP('',(#22309));
#6323=EDGE_LOOP('',(#22310));
#6324=EDGE_LOOP('',(#22311,#22312,#22313,#22314,#22315));
#6325=EDGE_LOOP('',(#22316));
#6326=EDGE_LOOP('',(#22317,#22318,#22319));
#6327=EDGE_LOOP('',(#22320,#22321,#22322));
#6328=EDGE_LOOP('',(#22323,#22324,#22325));
#6329=EDGE_LOOP('',(#22326,#22327,#22328));
#6330=EDGE_LOOP('',(#22329,#22330,#22331));
#6331=EDGE_LOOP('',(#22332,#22333,#22334));
#6332=EDGE_LOOP('',(#22335,#22336,#22337,#22338,#22339));
#6333=EDGE_LOOP('',(#22340,#22341,#22342,#22343,#22344));
#6334=EDGE_LOOP('',(#22345,#22346,#22347,#22348,#22349));
#6335=EDGE_LOOP('',(#22350,#22351,#22352,#22353,#22354,#22355));
#6336=EDGE_LOOP('',(#22356));
#6337=EDGE_LOOP('',(#22357,#22358,#22359,#22360,#22361));
#6338=EDGE_LOOP('',(#22362,#22363,#22364,#22365,#22366));
#6339=EDGE_LOOP('',(#22367,#22368,#22369,#22370,#22371));
#6340=EDGE_LOOP('',(#22372,#22373,#22374,#22375,#22376,#22377));
#6341=EDGE_LOOP('',(#22378,#22379,#22380,#22381));
#8525=LINE('',#51241,#11072);
#8526=LINE('',#51247,#11073);
#8527=LINE('',#51312,#11074);
#8528=LINE('',#51314,#11075);
#8529=LINE('',#51315,#11076);
#8530=LINE('',#51318,#11077);
#8531=LINE('',#51319,#11078);
#8532=LINE('',#51322,#11079);
#8533=LINE('',#51323,#11080);
#8534=LINE('',#51326,#11081);
#8535=LINE('',#51328,#11082);
#8536=LINE('',#51329,#11083);
#8537=LINE('',#51333,#11084);
#8538=LINE('',#51335,#11085);
#8539=LINE('',#51339,#11086);
#11072=VECTOR('',#39091,5.);
#11073=VECTOR('',#39098,4.5399125);
#11074=VECTOR('',#39129,10.);
#11075=VECTOR('',#39130,10.);
#11076=VECTOR('',#39131,10.);
#11077=VECTOR('',#39134,10.);
#11078=VECTOR('',#39135,10.);
#11079=VECTOR('',#39138,10.);
#11080=VECTOR('',#39139,10.);
#11081=VECTOR('',#39142,10.);
#11082=VECTOR('',#39143,10.);
#11083=VECTOR('',#39144,9.99999999999999);
#11084=VECTOR('',#39149,10.);
#11085=VECTOR('',#39152,10.);
#11086=VECTOR('',#39159,7.3);
#13698=VERTEX_POINT('',#51229);
#13699=VERTEX_POINT('',#51230);
#13700=VERTEX_POINT('',#51233);
#13701=VERTEX_POINT('',#51237);
#13702=VERTEX_POINT('',#51238);
#13703=VERTEX_POINT('',#51243);
#13704=VERTEX_POINT('',#51246);
#13705=VERTEX_POINT('',#51251);
#13706=VERTEX_POINT('',#51252);
#13707=VERTEX_POINT('',#51256);
#13708=VERTEX_POINT('',#51262);
#13709=VERTEX_POINT('',#51263);
#13710=VERTEX_POINT('',#51272);
#13711=VERTEX_POINT('',#51273);
#13712=VERTEX_POINT('',#51282);
#13713=VERTEX_POINT('',#51283);
#13714=VERTEX_POINT('',#51292);
#13715=VERTEX_POINT('',#51293);
#13716=VERTEX_POINT('',#51302);
#13717=VERTEX_POINT('',#51311);
#13718=VERTEX_POINT('',#51313);
#13719=VERTEX_POINT('',#51317);
#13720=VERTEX_POINT('',#51321);
#13721=VERTEX_POINT('',#51325);
#13722=VERTEX_POINT('',#51327);
#13723=VERTEX_POINT('',#51330);
#17051=EDGE_CURVE('',#13698,#13699,#2421,.T.);
#17052=EDGE_CURVE('',#13699,#13698,#2422,.T.);
#17053=EDGE_CURVE('',#13698,#13700,#2423,.T.);
#17054=EDGE_CURVE('',#13700,#13700,#2424,.T.);
#17055=EDGE_CURVE('',#13701,#13702,#2425,.T.);
#17056=EDGE_CURVE('',#13702,#13701,#2426,.T.);
#17057=EDGE_CURVE('',#13702,#13699,#8525,.T.);
#17058=EDGE_CURVE('',#13703,#13703,#2427,.T.);
#17059=EDGE_CURVE('',#13701,#13704,#8526,.T.);
#17060=EDGE_CURVE('',#13704,#13704,#2428,.T.);
#17061=EDGE_CURVE('',#13705,#13706,#497,.T.);
#17062=EDGE_CURVE('',#13707,#13705,#2429,.T.);
#17063=EDGE_CURVE('',#13706,#13707,#498,.T.);
#17064=EDGE_CURVE('',#13708,#13709,#499,.T.);
#17065=EDGE_CURVE('',#13707,#13708,#500,.T.);
#17066=EDGE_CURVE('',#13709,#13707,#2430,.T.);
#17067=EDGE_CURVE('',#13710,#13711,#501,.T.);
#17068=EDGE_CURVE('',#13705,#13710,#2431,.T.);
#17069=EDGE_CURVE('',#13711,#13705,#502,.T.);
#17070=EDGE_CURVE('',#13712,#13713,#503,.T.);
#17071=EDGE_CURVE('',#13709,#13712,#504,.T.);
#17072=EDGE_CURVE('',#13713,#13709,#2432,.T.);
#17073=EDGE_CURVE('',#13714,#13715,#505,.T.);
#17074=EDGE_CURVE('',#13710,#13714,#2433,.T.);
#17075=EDGE_CURVE('',#13715,#13710,#506,.T.);
#17076=EDGE_CURVE('',#13716,#13714,#507,.T.);
#17077=EDGE_CURVE('',#13713,#13716,#508,.T.);
#17078=EDGE_CURVE('',#13714,#13713,#2434,.T.);
#17079=EDGE_CURVE('',#13717,#13715,#8527,.T.);
#17080=EDGE_CURVE('',#13718,#13717,#8528,.T.);
#17081=EDGE_CURVE('',#13718,#13716,#8529,.T.);
#17082=EDGE_CURVE('',#13719,#13711,#8530,.T.);
#17083=EDGE_CURVE('',#13717,#13719,#8531,.T.);
#17084=EDGE_CURVE('',#13720,#13706,#8532,.T.);
#17085=EDGE_CURVE('',#13719,#13720,#8533,.T.);
#17086=EDGE_CURVE('',#13720,#13721,#8534,.T.);
#17087=EDGE_CURVE('',#13721,#13722,#8535,.T.);
#17088=EDGE_CURVE('',#13722,#13718,#8536,.T.);
#17089=EDGE_CURVE('',#13723,#13723,#2435,.T.);
#17090=EDGE_CURVE('',#13721,#13708,#8537,.T.);
#17091=EDGE_CURVE('',#13722,#13712,#8538,.T.);
#17092=EDGE_CURVE('',#13703,#13723,#8539,.T.);
#22298=ORIENTED_EDGE('',*,*,#17051,.T.);
#22299=ORIENTED_EDGE('',*,*,#17052,.T.);
#22300=ORIENTED_EDGE('',*,*,#17053,.T.);
#22301=ORIENTED_EDGE('',*,*,#17054,.T.);
#22302=ORIENTED_EDGE('',*,*,#17053,.F.);
#22303=ORIENTED_EDGE('',*,*,#17055,.F.);
#22304=ORIENTED_EDGE('',*,*,#17056,.F.);
#22305=ORIENTED_EDGE('',*,*,#17057,.T.);
#22306=ORIENTED_EDGE('',*,*,#17051,.F.);
#22307=ORIENTED_EDGE('',*,*,#17052,.F.);
#22308=ORIENTED_EDGE('',*,*,#17057,.F.);
#22309=ORIENTED_EDGE('',*,*,#17058,.T.);
#22310=ORIENTED_EDGE('',*,*,#17054,.F.);
#22311=ORIENTED_EDGE('',*,*,#17055,.T.);
#22312=ORIENTED_EDGE('',*,*,#17056,.T.);
#22313=ORIENTED_EDGE('',*,*,#17059,.T.);
#22314=ORIENTED_EDGE('',*,*,#17060,.T.);
#22315=ORIENTED_EDGE('',*,*,#17059,.F.);
#22316=ORIENTED_EDGE('',*,*,#17060,.F.);
#22317=ORIENTED_EDGE('',*,*,#17061,.F.);
#22318=ORIENTED_EDGE('',*,*,#17062,.F.);
#22319=ORIENTED_EDGE('',*,*,#17063,.F.);
#22320=ORIENTED_EDGE('',*,*,#17064,.F.);
#22321=ORIENTED_EDGE('',*,*,#17065,.F.);
#22322=ORIENTED_EDGE('',*,*,#17066,.F.);
#22323=ORIENTED_EDGE('',*,*,#17067,.F.);
#22324=ORIENTED_EDGE('',*,*,#17068,.F.);
#22325=ORIENTED_EDGE('',*,*,#17069,.F.);
#22326=ORIENTED_EDGE('',*,*,#17070,.F.);
#22327=ORIENTED_EDGE('',*,*,#17071,.F.);
#22328=ORIENTED_EDGE('',*,*,#17072,.F.);
#22329=ORIENTED_EDGE('',*,*,#17073,.F.);
#22330=ORIENTED_EDGE('',*,*,#17074,.F.);
#22331=ORIENTED_EDGE('',*,*,#17075,.F.);
#22332=ORIENTED_EDGE('',*,*,#17076,.F.);
#22333=ORIENTED_EDGE('',*,*,#17077,.F.);
#22334=ORIENTED_EDGE('',*,*,#17078,.F.);
#22335=ORIENTED_EDGE('',*,*,#17076,.T.);
#22336=ORIENTED_EDGE('',*,*,#17073,.T.);
#22337=ORIENTED_EDGE('',*,*,#17079,.F.);
#22338=ORIENTED_EDGE('',*,*,#17080,.F.);
#22339=ORIENTED_EDGE('',*,*,#17081,.T.);
#22340=ORIENTED_EDGE('',*,*,#17075,.T.);
#22341=ORIENTED_EDGE('',*,*,#17067,.T.);
#22342=ORIENTED_EDGE('',*,*,#17082,.F.);
#22343=ORIENTED_EDGE('',*,*,#17083,.F.);
#22344=ORIENTED_EDGE('',*,*,#17079,.T.);
#22345=ORIENTED_EDGE('',*,*,#17069,.T.);
#22346=ORIENTED_EDGE('',*,*,#17061,.T.);
#22347=ORIENTED_EDGE('',*,*,#17084,.F.);
#22348=ORIENTED_EDGE('',*,*,#17085,.F.);
#22349=ORIENTED_EDGE('',*,*,#17082,.T.);
#22350=ORIENTED_EDGE('',*,*,#17085,.T.);
#22351=ORIENTED_EDGE('',*,*,#17086,.T.);
#22352=ORIENTED_EDGE('',*,*,#17087,.T.);
#22353=ORIENTED_EDGE('',*,*,#17088,.T.);
#22354=ORIENTED_EDGE('',*,*,#17080,.T.);
#22355=ORIENTED_EDGE('',*,*,#17083,.T.);
#22356=ORIENTED_EDGE('',*,*,#17089,.F.);
#22357=ORIENTED_EDGE('',*,*,#17065,.T.);
#22358=ORIENTED_EDGE('',*,*,#17090,.F.);
#22359=ORIENTED_EDGE('',*,*,#17086,.F.);
#22360=ORIENTED_EDGE('',*,*,#17084,.T.);
#22361=ORIENTED_EDGE('',*,*,#17063,.T.);
#22362=ORIENTED_EDGE('',*,*,#17071,.T.);
#22363=ORIENTED_EDGE('',*,*,#17091,.F.);
#22364=ORIENTED_EDGE('',*,*,#17087,.F.);
#22365=ORIENTED_EDGE('',*,*,#17090,.T.);
#22366=ORIENTED_EDGE('',*,*,#17064,.T.);
#22367=ORIENTED_EDGE('',*,*,#17077,.T.);
#22368=ORIENTED_EDGE('',*,*,#17081,.F.);
#22369=ORIENTED_EDGE('',*,*,#17088,.F.);
#22370=ORIENTED_EDGE('',*,*,#17091,.T.);
#22371=ORIENTED_EDGE('',*,*,#17070,.T.);
#22372=ORIENTED_EDGE('',*,*,#17062,.T.);
#22373=ORIENTED_EDGE('',*,*,#17068,.T.);
#22374=ORIENTED_EDGE('',*,*,#17074,.T.);
#22375=ORIENTED_EDGE('',*,*,#17078,.T.);
#22376=ORIENTED_EDGE('',*,*,#17072,.T.);
#22377=ORIENTED_EDGE('',*,*,#17066,.T.);
#22378=ORIENTED_EDGE('',*,*,#17058,.F.);
#22379=ORIENTED_EDGE('',*,*,#17092,.T.);
#22380=ORIENTED_EDGE('',*,*,#17089,.T.);
#22381=ORIENTED_EDGE('',*,*,#17092,.F.);
#31178=PLANE('',#34485);
#31179=PLANE('',#34489);
#31180=PLANE('',#34502);
#31181=PLANE('',#34503);
#31182=PLANE('',#34504);
#31183=PLANE('',#34505);
#31184=PLANE('',#34507);
#31185=PLANE('',#34508);
#31186=PLANE('',#34509);
#31187=PLANE('',#34510);
#32098=ADVANCED_FACE('',(#4417),#894,.F.);
#32099=ADVANCED_FACE('',(#4418),#1099,.T.);
#32100=ADVANCED_FACE('',(#4419,#1903),#31178,.T.);
#32101=ADVANCED_FACE('',(#4420),#571,.T.);
#32102=ADVANCED_FACE('',(#4421),#31179,.T.);
#32103=ADVANCED_FACE('',(#4422),#572,.T.);
#32104=ADVANCED_FACE('',(#4423),#573,.T.);
#32105=ADVANCED_FACE('',(#4424),#574,.T.);
#32106=ADVANCED_FACE('',(#4425),#575,.T.);
#32107=ADVANCED_FACE('',(#4426),#576,.T.);
#32108=ADVANCED_FACE('',(#4427),#577,.T.);
#32109=ADVANCED_FACE('',(#4428),#31180,.T.);
#32110=ADVANCED_FACE('',(#4429),#31181,.T.);
#32111=ADVANCED_FACE('',(#4430),#31182,.T.);
#32112=ADVANCED_FACE('',(#4431,#1904),#31183,.T.);
#32113=ADVANCED_FACE('',(#4432),#31184,.T.);
#32114=ADVANCED_FACE('',(#4433),#31185,.T.);
#32115=ADVANCED_FACE('',(#4434),#31186,.T.);
#32116=ADVANCED_FACE('',(#4435),#31187,.F.);
#32117=ADVANCED_FACE('',(#4436),#1100,.T.);
#33796=CLOSED_SHELL('',(#32098,#32099,#32100,#32101,#32102,#32103,#32104,
#32105,#32106,#32107,#32108,#32109,#32110,#32111,#32112,#32113,#32114,#32115,
#32116,#32117));
#34476=AXIS2_PLACEMENT_3D('',#51227,#39073,#39074);
#34477=AXIS2_PLACEMENT_3D('',#51228,#39075,#39076);
#34478=AXIS2_PLACEMENT_3D('',#51231,#39077,#39078);
#34479=AXIS2_PLACEMENT_3D('',#51232,#39079,#39080);
#34480=AXIS2_PLACEMENT_3D('',#51234,#39081,#39082);
#34481=AXIS2_PLACEMENT_3D('',#51235,#39083,#39084);
#34482=AXIS2_PLACEMENT_3D('',#51236,#39085,#39086);
#34483=AXIS2_PLACEMENT_3D('',#51239,#39087,#39088);
#34484=AXIS2_PLACEMENT_3D('',#51240,#39089,#39090);
#34485=AXIS2_PLACEMENT_3D('',#51242,#39092,#39093);
#34486=AXIS2_PLACEMENT_3D('',#51244,#39094,#39095);
#34487=AXIS2_PLACEMENT_3D('',#51245,#39096,#39097);
#34488=AXIS2_PLACEMENT_3D('',#51248,#39099,#39100);
#34489=AXIS2_PLACEMENT_3D('',#51249,#39101,#39102);
#34490=AXIS2_PLACEMENT_3D('',#51250,#39103,#39104);
#34491=AXIS2_PLACEMENT_3D('',#51257,#39105,#39106);
#34492=AXIS2_PLACEMENT_3D('',#51261,#39107,#39108);
#34493=AXIS2_PLACEMENT_3D('',#51270,#39109,#39110);
#34494=AXIS2_PLACEMENT_3D('',#51271,#39111,#39112);
#34495=AXIS2_PLACEMENT_3D('',#51277,#39113,#39114);
#34496=AXIS2_PLACEMENT_3D('',#51281,#39115,#39116);
#34497=AXIS2_PLACEMENT_3D('',#51290,#39117,#39118);
#34498=AXIS2_PLACEMENT_3D('',#51291,#39119,#39120);
#34499=AXIS2_PLACEMENT_3D('',#51297,#39121,#39122);
#34500=AXIS2_PLACEMENT_3D('',#51301,#39123,#39124);
#34501=AXIS2_PLACEMENT_3D('',#51309,#39125,#39126);
#34502=AXIS2_PLACEMENT_3D('',#51310,#39127,#39128);
#34503=AXIS2_PLACEMENT_3D('',#51316,#39132,#39133);
#34504=AXIS2_PLACEMENT_3D('',#51320,#39136,#39137);
#34505=AXIS2_PLACEMENT_3D('',#51324,#39140,#39141);
#34506=AXIS2_PLACEMENT_3D('',#51331,#39145,#39146);
#34507=AXIS2_PLACEMENT_3D('',#51332,#39147,#39148);
#34508=AXIS2_PLACEMENT_3D('',#51334,#39150,#39151);
#34509=AXIS2_PLACEMENT_3D('',#51336,#39153,#39154);
#34510=AXIS2_PLACEMENT_3D('',#51337,#39155,#39156);
#34511=AXIS2_PLACEMENT_3D('',#51338,#39157,#39158);
#39073=DIRECTION('axis',(0.,0.,1.));
#39074=DIRECTION('refdir',(1.,0.,0.));
#39075=DIRECTION('center_axis',(-1.30103752480477E-16,7.77119338241477E-16,
-1.));
#39076=DIRECTION('ref_axis',(0.,-1.,0.));
#39077=DIRECTION('center_axis',(1.30103752480477E-16,-7.77119338241477E-16,
1.));
#39078=DIRECTION('ref_axis',(1.,1.22464679914733E-16,-1.30103752480477E-16));
#39079=DIRECTION('center_axis',(1.30103752480477E-16,-7.77119338241477E-16,
1.));
#39080=DIRECTION('ref_axis',(1.,1.22464679914733E-16,-1.30103752480477E-16));
#39081=DIRECTION('center_axis',(-1.,0.,1.30103752480477E-16));
#39082=DIRECTION('ref_axis',(0.,1.,0.));
#39083=DIRECTION('center_axis',(-1.30103752480477E-16,7.77119338241477E-16,
-1.));
#39084=DIRECTION('ref_axis',(1.,1.22464679914733E-16,-1.30103752480477E-16));
#39085=DIRECTION('center_axis',(-1.30103752480477E-16,7.77119338241477E-16,
-1.));
#39086=DIRECTION('ref_axis',(-1.,2.49761481516283E-30,1.30103752480477E-16));
#39087=DIRECTION('center_axis',(-1.30103752480477E-16,7.77119338241477E-16,
-1.));
#39088=DIRECTION('ref_axis',(1.,-2.49761481516283E-30,-1.30103752480477E-16));
#39089=DIRECTION('center_axis',(-1.30103752480477E-16,7.77119338241477E-16,
-1.));
#39090=DIRECTION('ref_axis',(1.,-2.49761481516283E-30,-1.30103752480477E-16));
#39091=DIRECTION('',(1.30103752480477E-16,-7.77119338241477E-16,1.));
#39092=DIRECTION('center_axis',(-1.30103752480477E-16,7.77119338241477E-16,
-1.));
#39093=DIRECTION('ref_axis',(-2.59872095719319E-30,-1.,-7.77119338241477E-16));
#39094=DIRECTION('center_axis',(-1.30103752480477E-16,7.77119338241477E-16,
-1.));
#39095=DIRECTION('ref_axis',(-1.,2.49761481516283E-30,1.30103752480477E-16));
#39096=DIRECTION('center_axis',(1.30103752480477E-16,-7.77119338241477E-16,
1.));
#39097=DIRECTION('ref_axis',(1.,-2.49761481516283E-30,-1.30103752480477E-16));
#39098=DIRECTION('',(0.707068359822735,6.36127110587822E-16,-0.70714520046281));
#39099=DIRECTION('center_axis',(1.30103752480477E-16,-7.77119338241477E-16,
1.));
#39100=DIRECTION('ref_axis',(1.,-2.49761481516283E-30,-1.30103752480477E-16));
#39101=DIRECTION('center_axis',(-1.30103752480477E-16,7.77119338241477E-16,
-1.));
#39102=DIRECTION('ref_axis',(-2.59872095719319E-30,-1.,-7.77119338241477E-16));
#39103=DIRECTION('center_axis',(1.92452000305188E-48,7.77119338241477E-16,
-1.));
#39104=DIRECTION('ref_axis',(-1.,2.59872095719319E-30,2.01759179052518E-45));
#39105=DIRECTION('center_axis',(1.30110639599212E-16,-7.76859649098367E-16,
1.));
#39106=DIRECTION('ref_axis',(-1.,2.49764325137018E-30,1.30110639599212E-16));
#39107=DIRECTION('center_axis',(1.92452000305188E-48,7.77119338241477E-16,
-1.));
#39108=DIRECTION('ref_axis',(-1.,2.59872095719319E-30,2.01759179052518E-45));
#39109=DIRECTION('center_axis',(1.30110639599212E-16,-7.76859649098367E-16,
1.));
#39110=DIRECTION('ref_axis',(-1.,2.49764325137018E-30,1.30110639599212E-16));
#39111=DIRECTION('center_axis',(1.92452000305188E-48,7.77119338241477E-16,
-1.));
#39112=DIRECTION('ref_axis',(-1.,2.59872095719319E-30,2.01759179052518E-45));
#39113=DIRECTION('center_axis',(1.30110639599212E-16,-7.76859649098367E-16,
1.));
#39114=DIRECTION('ref_axis',(-1.,2.49764325137018E-30,1.30110639599212E-16));
#39115=DIRECTION('center_axis',(1.92452000305188E-48,7.77119338241477E-16,
-1.));
#39116=DIRECTION('ref_axis',(1.,-1.89882151931499E-15,-1.47561092252874E-30));
#39117=DIRECTION('center_axis',(1.30110639599212E-16,-7.76859649098367E-16,
1.));
#39118=DIRECTION('ref_axis',(-1.,2.49764325137018E-30,1.30110639599212E-16));
#39119=DIRECTION('center_axis',(1.92452000305188E-48,7.77119338241477E-16,
-1.));
#39120=DIRECTION('ref_axis',(-1.,2.59872095719319E-30,2.01759179052518E-45));
#39121=DIRECTION('center_axis',(1.30110639599212E-16,-7.76859649098367E-16,
1.));
#39122=DIRECTION('ref_axis',(-1.,2.49764325137018E-30,1.30110639599212E-16));
#39123=DIRECTION('center_axis',(1.92452000305188E-48,7.77119338241477E-16,
-1.));
#39124=DIRECTION('ref_axis',(-1.,2.59872095719319E-30,2.01759179052518E-45));
#39125=DIRECTION('center_axis',(1.30110639599212E-16,-7.76859649098367E-16,
1.));
#39126=DIRECTION('ref_axis',(-1.,2.49764325137018E-30,1.30110639599212E-16));
#39127=DIRECTION('center_axis',(-3.60555503696922E-16,-1.,-7.77119338241477E-16));
#39128=DIRECTION('ref_axis',(2.2010686355983E-47,-7.77119338241477E-16,
1.));
#39129=DIRECTION('',(1.84116587831701E-16,-7.77119338241477E-16,1.));
#39130=DIRECTION('',(-1.,3.60555503696922E-16,1.30103752480477E-16));
#39131=DIRECTION('',(1.84116587831701E-16,-7.77119338241477E-16,1.));
#39132=DIRECTION('center_axis',(-0.866025403784439,-0.5,-2.29110026800376E-16));
#39133=DIRECTION('ref_axis',(-0.5,0.866025403784439,6.73005088689271E-16));
#39134=DIRECTION('',(1.84116587831701E-16,-7.77119338241477E-16,1.));
#39135=DIRECTION('',(-0.5,0.866025403784439,7.3805696492951E-16));
#39136=DIRECTION('center_axis',(-0.866025403784438,0.500000000000001,5.48009311441101E-16));
#39137=DIRECTION('ref_axis',(-1.72563323017096E-31,1.0960186228822E-15,
-1.));
#39138=DIRECTION('',(1.84116587831701E-16,-7.77119338241477E-16,1.));
#39139=DIRECTION('',(0.500000000000001,0.866025403784438,6.07953212449032E-16));
#39140=DIRECTION('center_axis',(-1.29960708002532E-16,7.77119338241477E-16,
-1.));
#39141=DIRECTION('ref_axis',(-2.59872095719319E-30,-1.,-7.77119338241477E-16));
#39142=DIRECTION('',(1.,-8.41296175292812E-16,-1.30103752480478E-16));
#39143=DIRECTION('',(0.499999999999999,-0.866025403784439,-7.3805696492951E-16));
#39144=DIRECTION('',(-0.5,-0.866025403784438,-6.07953212449032E-16));
#39145=DIRECTION('center_axis',(-1.30103752480477E-16,7.77119338241477E-16,
-1.));
#39146=DIRECTION('ref_axis',(-1.,2.49761481516283E-30,1.30103752480477E-16));
#39147=DIRECTION('center_axis',(8.41296175292813E-16,1.,7.77119338241477E-16));
#39148=DIRECTION('ref_axis',(-1.28389381285026E-46,7.77119338241477E-16,
-1.));
#39149=DIRECTION('',(1.84116587831701E-16,-7.77119338241477E-16,1.));
#39150=DIRECTION('center_axis',(0.866025403784439,0.5,2.29110026800376E-16));
#39151=DIRECTION('ref_axis',(0.5,-0.866025403784439,-6.73005088689271E-16));
#39152=DIRECTION('',(1.84116587831701E-16,-7.77119338241477E-16,1.));
#39153=DIRECTION('center_axis',(0.866025403784438,-0.5,-5.48009311441101E-16));
#39154=DIRECTION('ref_axis',(4.19082355898662E-31,-1.0960186228822E-15,
1.));
#39155=DIRECTION('center_axis',(-1.30110639599212E-16,7.76859649098367E-16,
-1.));
#39156=DIRECTION('ref_axis',(-2.59868716887268E-30,-1.,-7.76859649098367E-16));
#39157=DIRECTION('center_axis',(-1.30103752480477E-16,7.77119338241477E-16,
-1.));
#39158=DIRECTION('ref_axis',(-1.,2.49761481516283E-30,1.30103752480477E-16));
#39159=DIRECTION('',(1.30103752480477E-16,-7.77119338241477E-16,1.));
#51227=CARTESIAN_POINT('',(0.,0.,0.));
#51228=CARTESIAN_POINT('Origin',(444.115917770964,-290.472007268783,358.999900551893));
#51229=CARTESIAN_POINT('',(444.115917770964,-285.472007268783,358.999900551893));
#51230=CARTESIAN_POINT('',(449.115917770964,-290.472007268783,358.999900551893));
#51231=CARTESIAN_POINT('Origin',(444.115917770964,-290.472007268783,358.999900551893));
#51232=CARTESIAN_POINT('Origin',(444.115917770964,-290.472007268783,358.999900551893));
#51233=CARTESIAN_POINT('',(444.115917770964,-285.072007268783,359.399900551893));
#51234=CARTESIAN_POINT('Origin',(444.115917770964,-285.072007268783,358.999900551893));
#51235=CARTESIAN_POINT('Origin',(444.115917770964,-290.472007268783,359.399900551893));
#51236=CARTESIAN_POINT('Origin',(444.115917770964,-290.472007268783,344.649900551893));
#51237=CARTESIAN_POINT('',(439.115917770964,-290.472007268783,335.320175551893));
#51238=CARTESIAN_POINT('',(449.115917770964,-290.472007268783,335.320175551893));
#51239=CARTESIAN_POINT('Origin',(444.115917770964,-290.472007268783,335.320175551893));
#51240=CARTESIAN_POINT('Origin',(444.115917770964,-290.472007268783,335.320175551893));
#51241=CARTESIAN_POINT('',(449.115917770964,-290.472007268783,344.649900551893));
#51242=CARTESIAN_POINT('Origin',(437.965917770964,-290.472007268783,359.399900551893));
#51243=CARTESIAN_POINT('',(451.415917770964,-290.472007268783,359.399900551893));
#51244=CARTESIAN_POINT('Origin',(444.115917770964,-290.472007268783,359.399900551893));
#51245=CARTESIAN_POINT('Origin',(444.115917770964,-290.472007268783,334.860038051893));
#51246=CARTESIAN_POINT('',(440.036092770964,-290.472007268783,334.399900551893));
#51247=CARTESIAN_POINT('',(439.576005270964,-290.472007268783,334.860038051893));
#51248=CARTESIAN_POINT('Origin',(444.115917770964,-290.472007268783,334.399900551893));
#51249=CARTESIAN_POINT('Origin',(441.615917770964,-290.472007268783,334.399900551893));
#51250=CARTESIAN_POINT('Origin',(444.115917770964,-290.472007268783,365.672734961985));
#51251=CARTESIAN_POINT('',(437.187714540689,-286.472007268783,366.030000551893));
#51252=CARTESIAN_POINT('',(439.497115617447,-282.472007268783,365.315469372077));
#51253=CARTESIAN_POINT('Ctrl Pts',(437.187714540689,-286.472007268783,366.030000551893));
#51254=CARTESIAN_POINT('Ctrl Pts',(438.259511310413,-284.615600808232,366.030000551893));
#51255=CARTESIAN_POINT('Ctrl Pts',(439.497115617447,-282.472007268783,365.315469372077));
#51256=CARTESIAN_POINT('',(444.115917770964,-282.472007268783,366.030000551893));
#51257=CARTESIAN_POINT('Origin',(444.115917770964,-290.472007268783,366.030000551893));
#51258=CARTESIAN_POINT('Ctrl Pts',(439.497115617447,-282.472007268783,365.315469372077));
#51259=CARTESIAN_POINT('Ctrl Pts',(441.972324231515,-282.472007268783,366.030000551893));
#51260=CARTESIAN_POINT('Ctrl Pts',(444.115917770964,-282.472007268783,366.030000551893));
#51261=CARTESIAN_POINT('Origin',(444.115917770964,-290.472007268783,365.672734961985));
#51262=CARTESIAN_POINT('',(448.734719924481,-282.472007268783,365.315469372077));
#51263=CARTESIAN_POINT('',(451.04412100124,-286.472007268783,366.030000551893));
#51264=CARTESIAN_POINT('Ctrl Pts',(448.734719924481,-282.472007268783,365.315469372077));
#51265=CARTESIAN_POINT('Ctrl Pts',(449.972324231515,-284.615600808232,366.030000551893));
#51266=CARTESIAN_POINT('Ctrl Pts',(451.04412100124,-286.472007268783,366.030000551893));
#51267=CARTESIAN_POINT('Ctrl Pts',(444.115917770964,-282.472007268783,366.030000551893));
#51268=CARTESIAN_POINT('Ctrl Pts',(446.259511310413,-282.472007268783,366.030000551893));
#51269=CARTESIAN_POINT('Ctrl Pts',(448.734719924481,-282.472007268783,365.315469372077));
#51270=CARTESIAN_POINT('Origin',(444.115917770964,-290.472007268783,366.030000551893));
#51271=CARTESIAN_POINT('Origin',(444.115917770964,-290.472007268783,365.672734961985));
#51272=CARTESIAN_POINT('',(437.187714540689,-294.472007268783,366.030000551893));
#51273=CARTESIAN_POINT('',(434.87831346393,-290.472007268783,365.315469372077));
#51274=CARTESIAN_POINT('Ctrl Pts',(437.187714540689,-294.472007268783,366.030000551893));
#51275=CARTESIAN_POINT('Ctrl Pts',(436.115917770964,-292.615600808232,366.030000551893));
#51276=CARTESIAN_POINT('Ctrl Pts',(434.87831346393,-290.472007268783,365.315469372077));
#51277=CARTESIAN_POINT('Origin',(444.115917770964,-290.472007268783,366.030000551893));
#51278=CARTESIAN_POINT('Ctrl Pts',(434.87831346393,-290.472007268783,365.315469372077));
#51279=CARTESIAN_POINT('Ctrl Pts',(436.115917770964,-288.328413729334,366.030000551893));
#51280=CARTESIAN_POINT('Ctrl Pts',(437.187714540689,-286.472007268783,366.030000551893));
#51281=CARTESIAN_POINT('Origin',(444.115917770964,-290.472007268783,365.672734961985));
#51282=CARTESIAN_POINT('',(453.353522077998,-290.472007268783,365.315469372077));
#51283=CARTESIAN_POINT('',(451.04412100124,-294.472007268783,366.030000551893));
#51284=CARTESIAN_POINT('Ctrl Pts',(453.353522077998,-290.472007268783,365.315469372077));
#51285=CARTESIAN_POINT('Ctrl Pts',(452.115917770964,-292.615600808232,366.030000551893));
#51286=CARTESIAN_POINT('Ctrl Pts',(451.04412100124,-294.472007268783,366.030000551893));
#51287=CARTESIAN_POINT('Ctrl Pts',(451.04412100124,-286.472007268783,366.030000551893));
#51288=CARTESIAN_POINT('Ctrl Pts',(452.115917770964,-288.328413729334,366.030000551893));
#51289=CARTESIAN_POINT('Ctrl Pts',(453.353522077998,-290.472007268783,365.315469372077));
#51290=CARTESIAN_POINT('Origin',(444.115917770964,-290.472007268783,366.030000551893));
#51291=CARTESIAN_POINT('Origin',(444.115917770964,-290.472007268783,365.672734961985));
#51292=CARTESIAN_POINT('',(444.115917770964,-298.472007268783,366.030000551893));
#51293=CARTESIAN_POINT('',(439.497115617447,-298.472007268783,365.315469372077));
#51294=CARTESIAN_POINT('Ctrl Pts',(444.115917770964,-298.472007268783,366.030000551893));
#51295=CARTESIAN_POINT('Ctrl Pts',(441.972324231515,-298.472007268783,366.030000551893));
#51296=CARTESIAN_POINT('Ctrl Pts',(439.497115617447,-298.472007268783,365.315469372077));
#51297=CARTESIAN_POINT('Origin',(444.115917770964,-290.472007268783,366.030000551893));
#51298=CARTESIAN_POINT('Ctrl Pts',(439.497115617447,-298.472007268783,365.315469372077));
#51299=CARTESIAN_POINT('Ctrl Pts',(438.259511310413,-296.328413729334,366.030000551893));
#51300=CARTESIAN_POINT('Ctrl Pts',(437.187714540689,-294.472007268783,366.030000551893));
#51301=CARTESIAN_POINT('Origin',(444.115917770964,-290.472007268783,365.672734961985));
#51302=CARTESIAN_POINT('',(448.734719924481,-298.472007268783,365.315469372077));
#51303=CARTESIAN_POINT('Ctrl Pts',(448.734719924481,-298.472007268783,365.315469372077));
#51304=CARTESIAN_POINT('Ctrl Pts',(446.259511310413,-298.472007268783,366.030000551893));
#51305=CARTESIAN_POINT('Ctrl Pts',(444.115917770964,-298.472007268783,366.030000551893));
#51306=CARTESIAN_POINT('Ctrl Pts',(451.04412100124,-294.472007268783,366.030000551893));
#51307=CARTESIAN_POINT('Ctrl Pts',(449.972324231515,-296.328413729334,366.030000551893));
#51308=CARTESIAN_POINT('Ctrl Pts',(448.734719924481,-298.472007268783,365.315469372077));
#51309=CARTESIAN_POINT('Origin',(444.115917770964,-290.472007268783,366.030000551893));
#51310=CARTESIAN_POINT('Origin',(448.734719924481,-298.472007268783,360.000000551893));
#51311=CARTESIAN_POINT('',(439.497115617447,-298.472007268783,360.000000551893));
#51312=CARTESIAN_POINT('',(439.497115617447,-298.472007268783,360.000000551893));
#51313=CARTESIAN_POINT('',(448.734719924481,-298.472007268783,360.000000551893));
#51314=CARTESIAN_POINT('',(448.734719924481,-298.472007268783,360.000000551893));
#51315=CARTESIAN_POINT('',(448.734719924481,-298.472007268783,360.000000551893));
#51316=CARTESIAN_POINT('Origin',(439.497115617447,-298.472007268783,360.000000551893));
#51317=CARTESIAN_POINT('',(434.87831346393,-290.472007268783,360.000000551893));
#51318=CARTESIAN_POINT('',(434.87831346393,-290.472007268783,360.000000551893));
#51319=CARTESIAN_POINT('',(439.497115617447,-298.472007268783,360.000000551893));
#51320=CARTESIAN_POINT('Origin',(434.87831346393,-290.472007268783,360.000000551893));
#51321=CARTESIAN_POINT('',(439.497115617447,-282.472007268783,360.000000551893));
#51322=CARTESIAN_POINT('',(439.497115617447,-282.472007268783,360.000000551893));
#51323=CARTESIAN_POINT('',(434.87831346393,-290.472007268783,360.000000551893));
#51324=CARTESIAN_POINT('Origin',(444.115917770964,-290.472007268783,360.000000551893));
#51325=CARTESIAN_POINT('',(448.734719924481,-282.472007268783,360.000000551893));
#51326=CARTESIAN_POINT('',(439.497115617447,-282.472007268783,360.000000551893));
#51327=CARTESIAN_POINT('',(453.353522077998,-290.472007268783,360.000000551893));
#51328=CARTESIAN_POINT('',(448.734719924481,-282.472007268783,360.000000551893));
#51329=CARTESIAN_POINT('',(453.353522077998,-290.472007268783,360.000000551893));
#51330=CARTESIAN_POINT('',(451.415917770964,-290.472007268783,360.000000551893));
#51331=CARTESIAN_POINT('Origin',(444.115917770964,-290.472007268783,360.000000551893));
#51332=CARTESIAN_POINT('Origin',(439.497115617447,-282.472007268783,360.000000551893));
#51333=CARTESIAN_POINT('',(448.734719924481,-282.472007268783,360.000000551893));
#51334=CARTESIAN_POINT('Origin',(448.734719924481,-282.472007268783,360.000000551893));
#51335=CARTESIAN_POINT('',(453.353522077998,-290.472007268783,360.000000551893));
#51336=CARTESIAN_POINT('Origin',(453.353522077998,-290.472007268783,360.000000551893));
#51337=CARTESIAN_POINT('Origin',(444.115917770964,-290.472007268783,366.030000551893));
#51338=CARTESIAN_POINT('Origin',(444.115917770964,-290.472007268783,359.699950551893));
#51339=CARTESIAN_POINT('',(451.415917770964,-290.472007268783,359.699950551893));
#61756=UNCERTAINTY_MEASURE_WITH_UNIT(LENGTH_MEASURE(0.01),#61812,
'DISTANCE_ACCURACY_VALUE',
'Maximum model space distance between geometric entities at asserted c
onnectivities');
#61780=UNCERTAINTY_MEASURE_WITH_UNIT(LENGTH_MEASURE(0.01),#61812,
'DISTANCE_ACCURACY_VALUE',
'Maximum model space distance between geometric entities at asserted c
onnectivities');
#61787=(
GEOMETRIC_REPRESENTATION_CONTEXT(3)
GLOBAL_UNCERTAINTY_ASSIGNED_CONTEXT((#61756))
GLOBAL_UNIT_ASSIGNED_CONTEXT((#61812,#61814,#61815))
REPRESENTATION_CONTEXT('','3D')
);
#61811=(
GEOMETRIC_REPRESENTATION_CONTEXT(3)
GLOBAL_UNCERTAINTY_ASSIGNED_CONTEXT((#61780))
GLOBAL_UNIT_ASSIGNED_CONTEXT((#61812,#61814,#61815))
REPRESENTATION_CONTEXT('','3D')
);
#61812=(
LENGTH_UNIT()
NAMED_UNIT(*)
SI_UNIT(.MILLI.,.METRE.)
);
#61814=(
NAMED_UNIT(*)
PLANE_ANGLE_UNIT()
SI_UNIT($,.RADIAN.)
);
#61815=(
NAMED_UNIT(*)
SI_UNIT($,.STERADIAN.)
SOLID_ANGLE_UNIT()
);
#61822=SHAPE_DEFINITION_REPRESENTATION(#61852,#61974);
#61852=PRODUCT_DEFINITION_SHAPE('',$,#62005);
#61974=SHAPE_REPRESENTATION('',(#34476),#61787);
#61998=PRODUCT_DEFINITION_CONTEXT('part definition',#62090,'design');
#62005=PRODUCT_DEFINITION('Chamber Hex Head Bolts',
'Chamber Hex Head Bolts',#62035,#61998);
#62035=PRODUCT_DEFINITION_FORMATION('',$,#62098);
#62090=APPLICATION_CONTEXT('Managed model based 3d engineering');
#62091=PRODUCT_CONTEXT('part definition',#62090,'mechanical');
#62098=PRODUCT('Chamber Hex Head Bolts','Chamber Hex Head Bolts',$,(#62091));
#62157=COLOUR_RGB('Black',0.12,0.14,0.17);
#62158=FILL_AREA_STYLE_COLOUR('',#62157);
#62159=FILL_AREA_STYLE('',(#62158));
#62160=SURFACE_STYLE_FILL_AREA(#62159);
#62161=SURFACE_SIDE_STYLE('',(#62160));
#62162=SURFACE_STYLE_USAGE(.BOTH.,#62161);
#62163=PRESENTATION_STYLE_ASSIGNMENT((#62162));
ENDSEC;
END-ISO-10303-21;
